ISO-10303-21;
HEADER;
/* Generated by software containing ST-Developer
 * from STEP Tools, Inc. (www.steptools.com) 
 */

FILE_DESCRIPTION(
/* description */ (''),
/* implementation_level */ '2;1');

FILE_NAME(
/* name */ 'Nut_01.step',
/* time_stamp */ '2026-10-06T13:15:55-07:00',
/* author */ (''),
/* organization */ (''),
/* preprocessor_version */ 'ST-DEVELOPER v20.2',
/* originating_system */ 'Autodesk Translation Framework v15.15.0.0',
/* authorisation */ '');

FILE_SCHEMA (('AUTOMOTIVE_DESIGN { 1 0 10303 214 3 1 1 }'));
ENDSEC;

DATA;
#10=MECHANICAL_DESIGN_GEOMETRIC_PRESENTATION_REPRESENTATION('',(#108),#27707);
#88=SHAPE_REPRESENTATION_RELATIONSHIP('SRR','None',#27745,#98);
#98=ADVANCED_BREP_SHAPE_REPRESENTATION('',(#118),#27697);
#108=STYLED_ITEM('',(#27804),#118);
#118=MANIFOLD_SOLID_BREP('Body1',#3834);
#128=FACE_BOUND('',#670,.T.);
#129=FACE_BOUND('',#672,.T.);
#163=PLANE('',#3963);
#164=PLANE('',#3964);
#165=PLANE('',#3965);
#166=PLANE('',#3966);
#167=PLANE('',#3967);
#168=PLANE('',#3968);
#169=PLANE('',#3969);
#170=PLANE('',#3970);
#218=CIRCLE('',#3958,4.433);
#219=CIRCLE('',#3959,4.433);
#220=CIRCLE('',#3961,3.72275);
#221=CIRCLE('',#3962,3.72275);
#344=CYLINDRICAL_SURFACE('',#3957,4.433);
#345=CYLINDRICAL_SURFACE('',#3960,3.72275);
#438=FACE_OUTER_BOUND('',#659,.T.);
#439=FACE_OUTER_BOUND('',#660,.T.);
#440=FACE_OUTER_BOUND('',#661,.T.);
#441=FACE_OUTER_BOUND('',#662,.T.);
#442=FACE_OUTER_BOUND('',#663,.T.);
#443=FACE_OUTER_BOUND('',#664,.T.);
#444=FACE_OUTER_BOUND('',#665,.T.);
#445=FACE_OUTER_BOUND('',#666,.T.);
#446=FACE_OUTER_BOUND('',#667,.T.);
#447=FACE_OUTER_BOUND('',#668,.T.);
#448=FACE_OUTER_BOUND('',#669,.T.);
#449=FACE_OUTER_BOUND('',#671,.T.);
#659=EDGE_LOOP('',(#2457,#2458,#2459,#2460));
#660=EDGE_LOOP('',(#2461,#2462,#2463,#2464));
#661=EDGE_LOOP('',(#2465,#2466,#2467,#2468));
#662=EDGE_LOOP('',(#2469,#2470,#2471,#2472));
#663=EDGE_LOOP('',(#2473,#2474,#2475,#2476));
#664=EDGE_LOOP('',(#2477,#2478,#2479,#2480));
#665=EDGE_LOOP('',(#2481,#2482,#2483,#2484));
#666=EDGE_LOOP('',(#2485,#2486,#2487,#2488));
#667=EDGE_LOOP('',(#2489,#2490,#2491,#2492));
#668=EDGE_LOOP('',(#2493,#2494,#2495,#2496));
#669=EDGE_LOOP('',(#2497,#2498,#2499,#2500,#2501,#2502));
#670=EDGE_LOOP('',(#2503,#2504,#2505,#2506));
#671=EDGE_LOOP('',(#2507,#2508,#2509,#2510,#2511,#2512));
#672=EDGE_LOOP('',(#2513,#2514,#2515,#2516));
#915=LINE('',#5177,#1091);
#916=LINE('',#5193,#1092);
#917=LINE('',#5199,#1093);
#918=LINE('',#5258,#1094);
#919=LINE('',#5265,#1095);
#920=LINE('',#5267,#1096);
#921=LINE('',#5269,#1097);
#922=LINE('',#5270,#1098);
#923=LINE('',#5273,#1099);
#924=LINE('',#5275,#1100);
#925=LINE('',#5276,#1101);
#926=LINE('',#5279,#1102);
#927=LINE('',#5281,#1103);
#928=LINE('',#5282,#1104);
#929=LINE('',#5285,#1105);
#930=LINE('',#5287,#1106);
#931=LINE('',#5288,#1107);
#932=LINE('',#5291,#1108);
#933=LINE('',#5293,#1109);
#934=LINE('',#5294,#1110);
#935=LINE('',#5296,#1111);
#936=LINE('',#5297,#1112);
#1091=VECTOR('',#4292,10.);
#1092=VECTOR('',#4293,10.);
#1093=VECTOR('',#4300,10.);
#1094=VECTOR('',#4301,10.);
#1095=VECTOR('',#4310,10.);
#1096=VECTOR('',#4311,10.);
#1097=VECTOR('',#4312,10.);
#1098=VECTOR('',#4313,10.);
#1099=VECTOR('',#4316,9.99999999999998);
#1100=VECTOR('',#4317,9.99999999999998);
#1101=VECTOR('',#4318,10.);
#1102=VECTOR('',#4321,10.);
#1103=VECTOR('',#4322,10.);
#1104=VECTOR('',#4323,10.);
#1105=VECTOR('',#4326,10.);
#1106=VECTOR('',#4327,10.);
#1107=VECTOR('',#4328,10.);
#1108=VECTOR('',#4331,10.);
#1109=VECTOR('',#4332,10.);
#1110=VECTOR('',#4333,10.);
#1111=VECTOR('',#4336,10.);
#1112=VECTOR('',#4337,10.);
#1267=B_SPLINE_CURVE_WITH_KNOTS('',3,(#5162,#5163,#5164,#5165,#5166,#5167,
#5168,#5169,#5170,#5171,#5172,#5173,#5174,#5175),.UNSPECIFIED.,.F.,.F.,
(4,2,2,2,2,2,4),(-0.844212290556731,-0.730966332817565,-0.619975754240938,
-0.457326579004558,-0.29977928179387,-0.147336283383114,0.),
 .UNSPECIFIED.);
#1268=B_SPLINE_CURVE_WITH_KNOTS('',3,(#5179,#5180,#5181,#5182,#5183,#5184,
#5185,#5186,#5187,#5188,#5189,#5190,#5191,#5192),.UNSPECIFIED.,.F.,.F.,
(4,2,2,2,2,2,4),(-0.844212290556731,-0.730966332817565,-0.619975754240938,
-0.457326579004558,-0.29977928179387,-0.147336283383114,0.),
 .UNSPECIFIED.);
#1269=B_SPLINE_CURVE_WITH_KNOTS('',3,(#5229,#5230,#5231,#5232,#5233,#5234,
#5235,#5236,#5237,#5238,#5239,#5240,#5241,#5242),.UNSPECIFIED.,.F.,.F.,
(4,2,2,2,2,2,4),(-0.847325527525843,-0.749719327139836,-0.649860858750851,
-0.495073659399383,-0.335166304629316,-0.170141007879843,0.),
 .UNSPECIFIED.);
#1270=B_SPLINE_CURVE_WITH_KNOTS('',3,(#5244,#5245,#5246,#5247,#5248,#5249,
#5250,#5251,#5252,#5253,#5254,#5255,#5256,#5257),.UNSPECIFIED.,.F.,.F.,
(4,2,2,2,2,2,4),(-0.847325527525843,-0.749719327139836,-0.649860858750851,
-0.495073659399383,-0.335166304629316,-0.170141007879843,0.),
 .UNSPECIFIED.);
#1521=VERTEX_POINT('',#5160);
#1522=VERTEX_POINT('',#5161);
#1523=VERTEX_POINT('',#5176);
#1524=VERTEX_POINT('',#5178);
#1525=VERTEX_POINT('',#5195);
#1526=VERTEX_POINT('',#5197);
#1527=VERTEX_POINT('',#5228);
#1528=VERTEX_POINT('',#5243);
#1529=VERTEX_POINT('',#5263);
#1530=VERTEX_POINT('',#5264);
#1531=VERTEX_POINT('',#5266);
#1532=VERTEX_POINT('',#5268);
#1533=VERTEX_POINT('',#5272);
#1534=VERTEX_POINT('',#5274);
#1535=VERTEX_POINT('',#5278);
#1536=VERTEX_POINT('',#5280);
#1537=VERTEX_POINT('',#5284);
#1538=VERTEX_POINT('',#5286);
#1539=VERTEX_POINT('',#5290);
#1540=VERTEX_POINT('',#5292);
#1898=EDGE_CURVE('',#1521,#1522,#1267,.T.);
#1899=EDGE_CURVE('',#1522,#1523,#915,.T.);
#1900=EDGE_CURVE('',#1524,#1523,#1268,.T.);
#1901=EDGE_CURVE('',#1521,#1524,#916,.T.);
#1902=EDGE_CURVE('',#1525,#1521,#218,.T.);
#1903=EDGE_CURVE('',#1526,#1524,#219,.T.);
#1904=EDGE_CURVE('',#1525,#1526,#917,.T.);
#1905=EDGE_CURVE('',#1527,#1525,#1269,.T.);
#1906=EDGE_CURVE('',#1528,#1526,#1270,.T.);
#1907=EDGE_CURVE('',#1527,#1528,#918,.T.);
#1908=EDGE_CURVE('',#1522,#1527,#220,.T.);
#1909=EDGE_CURVE('',#1523,#1528,#221,.T.);
#1910=EDGE_CURVE('',#1529,#1530,#919,.T.);
#1911=EDGE_CURVE('',#1530,#1531,#920,.T.);
#1912=EDGE_CURVE('',#1532,#1531,#921,.T.);
#1913=EDGE_CURVE('',#1529,#1532,#922,.T.);
#1914=EDGE_CURVE('',#1533,#1529,#923,.T.);
#1915=EDGE_CURVE('',#1534,#1532,#924,.T.);
#1916=EDGE_CURVE('',#1533,#1534,#925,.T.);
#1917=EDGE_CURVE('',#1535,#1533,#926,.T.);
#1918=EDGE_CURVE('',#1536,#1534,#927,.T.);
#1919=EDGE_CURVE('',#1535,#1536,#928,.T.);
#1920=EDGE_CURVE('',#1537,#1535,#929,.T.);
#1921=EDGE_CURVE('',#1538,#1536,#930,.T.);
#1922=EDGE_CURVE('',#1537,#1538,#931,.T.);
#1923=EDGE_CURVE('',#1539,#1537,#932,.T.);
#1924=EDGE_CURVE('',#1540,#1538,#933,.T.);
#1925=EDGE_CURVE('',#1539,#1540,#934,.T.);
#1926=EDGE_CURVE('',#1530,#1539,#935,.T.);
#1927=EDGE_CURVE('',#1531,#1540,#936,.T.);
#2457=ORIENTED_EDGE('',*,*,#1898,.T.);
#2458=ORIENTED_EDGE('',*,*,#1899,.T.);
#2459=ORIENTED_EDGE('',*,*,#1900,.F.);
#2460=ORIENTED_EDGE('',*,*,#1901,.F.);
#2461=ORIENTED_EDGE('',*,*,#1902,.T.);
#2462=ORIENTED_EDGE('',*,*,#1901,.T.);
#2463=ORIENTED_EDGE('',*,*,#1903,.F.);
#2464=ORIENTED_EDGE('',*,*,#1904,.F.);
#2465=ORIENTED_EDGE('',*,*,#1905,.T.);
#2466=ORIENTED_EDGE('',*,*,#1904,.T.);
#2467=ORIENTED_EDGE('',*,*,#1906,.F.);
#2468=ORIENTED_EDGE('',*,*,#1907,.F.);
#2469=ORIENTED_EDGE('',*,*,#1908,.T.);
#2470=ORIENTED_EDGE('',*,*,#1907,.T.);
#2471=ORIENTED_EDGE('',*,*,#1909,.F.);
#2472=ORIENTED_EDGE('',*,*,#1899,.F.);
#2473=ORIENTED_EDGE('',*,*,#1910,.T.);
#2474=ORIENTED_EDGE('',*,*,#1911,.T.);
#2475=ORIENTED_EDGE('',*,*,#1912,.F.);
#2476=ORIENTED_EDGE('',*,*,#1913,.F.);
#2477=ORIENTED_EDGE('',*,*,#1914,.T.);
#2478=ORIENTED_EDGE('',*,*,#1913,.T.);
#2479=ORIENTED_EDGE('',*,*,#1915,.F.);
#2480=ORIENTED_EDGE('',*,*,#1916,.F.);
#2481=ORIENTED_EDGE('',*,*,#1917,.T.);
#2482=ORIENTED_EDGE('',*,*,#1916,.T.);
#2483=ORIENTED_EDGE('',*,*,#1918,.F.);
#2484=ORIENTED_EDGE('',*,*,#1919,.F.);
#2485=ORIENTED_EDGE('',*,*,#1920,.T.);
#2486=ORIENTED_EDGE('',*,*,#1919,.T.);
#2487=ORIENTED_EDGE('',*,*,#1921,.F.);
#2488=ORIENTED_EDGE('',*,*,#1922,.F.);
#2489=ORIENTED_EDGE('',*,*,#1923,.T.);
#2490=ORIENTED_EDGE('',*,*,#1922,.T.);
#2491=ORIENTED_EDGE('',*,*,#1924,.F.);
#2492=ORIENTED_EDGE('',*,*,#1925,.F.);
#2493=ORIENTED_EDGE('',*,*,#1926,.T.);
#2494=ORIENTED_EDGE('',*,*,#1925,.T.);
#2495=ORIENTED_EDGE('',*,*,#1927,.F.);
#2496=ORIENTED_EDGE('',*,*,#1911,.F.);
#2497=ORIENTED_EDGE('',*,*,#1927,.T.);
#2498=ORIENTED_EDGE('',*,*,#1924,.T.);
#2499=ORIENTED_EDGE('',*,*,#1921,.T.);
#2500=ORIENTED_EDGE('',*,*,#1918,.T.);
#2501=ORIENTED_EDGE('',*,*,#1915,.T.);
#2502=ORIENTED_EDGE('',*,*,#1912,.T.);
#2503=ORIENTED_EDGE('',*,*,#1909,.T.);
#2504=ORIENTED_EDGE('',*,*,#1906,.T.);
#2505=ORIENTED_EDGE('',*,*,#1903,.T.);
#2506=ORIENTED_EDGE('',*,*,#1900,.T.);
#2507=ORIENTED_EDGE('',*,*,#1926,.F.);
#2508=ORIENTED_EDGE('',*,*,#1910,.F.);
#2509=ORIENTED_EDGE('',*,*,#1914,.F.);
#2510=ORIENTED_EDGE('',*,*,#1917,.F.);
#2511=ORIENTED_EDGE('',*,*,#1920,.F.);
#2512=ORIENTED_EDGE('',*,*,#1923,.F.);
#2513=ORIENTED_EDGE('',*,*,#1908,.F.);
#2514=ORIENTED_EDGE('',*,*,#1898,.F.);
#2515=ORIENTED_EDGE('',*,*,#1902,.F.);
#2516=ORIENTED_EDGE('',*,*,#1905,.F.);
#3575=B_SPLINE_SURFACE_WITH_KNOTS('',3,1,((#5132,#5133),(#5134,#5135),(#5136,
#5137),(#5138,#5139),(#5140,#5141),(#5142,#5143),(#5144,#5145),(#5146,#5147),
(#5148,#5149),(#5150,#5151),(#5152,#5153),(#5154,#5155),(#5156,#5157),(#5158,
#5159)),.UNSPECIFIED.,.F.,.F.,.F.,(4,2,2,2,2,2,4),(2,2),(-0.844212290556731,
-0.730966332817565,-0.619975754240938,-0.457326579004558,-0.29977928179387,
-0.147336283383114,0.),(0.,0.575999999999998),.UNSPECIFIED.);
#3576=B_SPLINE_SURFACE_WITH_KNOTS('',3,1,((#5200,#5201),(#5202,#5203),(#5204,
#5205),(#5206,#5207),(#5208,#5209),(#5210,#5211),(#5212,#5213),(#5214,#5215),
(#5216,#5217),(#5218,#5219),(#5220,#5221),(#5222,#5223),(#5224,#5225),(#5226,
#5227)),.UNSPECIFIED.,.F.,.F.,.F.,(4,2,2,2,2,2,4),(2,2),(-0.847325527525843,
-0.749719327139836,-0.649860858750851,-0.495073659399383,-0.335166304629316,
-0.170141007879843,0.),(0.,0.575999999999998),.UNSPECIFIED.);
#3613=ADVANCED_FACE('',(#438),#3575,.T.);
#3614=ADVANCED_FACE('',(#439),#344,.F.);
#3615=ADVANCED_FACE('',(#440),#3576,.T.);
#3616=ADVANCED_FACE('',(#441),#345,.F.);
#3617=ADVANCED_FACE('',(#442),#163,.T.);
#3618=ADVANCED_FACE('',(#443),#164,.T.);
#3619=ADVANCED_FACE('',(#444),#165,.T.);
#3620=ADVANCED_FACE('',(#445),#166,.T.);
#3621=ADVANCED_FACE('',(#446),#167,.T.);
#3622=ADVANCED_FACE('',(#447),#168,.T.);
#3623=ADVANCED_FACE('',(#448,#128),#169,.T.);
#3624=ADVANCED_FACE('',(#449,#129),#170,.F.);
#3834=CLOSED_SHELL('',(#3613,#3614,#3615,#3616,#3617,#3618,#3619,#3620,
#3621,#3622,#3623,#3624));
#3956=AXIS2_PLACEMENT_3D('',#5131,#4290,#4291);
#3957=AXIS2_PLACEMENT_3D('',#5194,#4294,#4295);
#3958=AXIS2_PLACEMENT_3D('',#5196,#4296,#4297);
#3959=AXIS2_PLACEMENT_3D('',#5198,#4298,#4299);
#3960=AXIS2_PLACEMENT_3D('',#5259,#4302,#4303);
#3961=AXIS2_PLACEMENT_3D('',#5260,#4304,#4305);
#3962=AXIS2_PLACEMENT_3D('',#5261,#4306,#4307);
#3963=AXIS2_PLACEMENT_3D('',#5262,#4308,#4309);
#3964=AXIS2_PLACEMENT_3D('',#5271,#4314,#4315);
#3965=AXIS2_PLACEMENT_3D('',#5277,#4319,#4320);
#3966=AXIS2_PLACEMENT_3D('',#5283,#4324,#4325);
#3967=AXIS2_PLACEMENT_3D('',#5289,#4329,#4330);
#3968=AXIS2_PLACEMENT_3D('',#5295,#4334,#4335);
#3969=AXIS2_PLACEMENT_3D('',#5298,#4338,#4339);
#3970=AXIS2_PLACEMENT_3D('',#5299,#4340,#4341);
#4290=DIRECTION('axis',(0.,0.,1.));
#4291=DIRECTION('refdir',(1.,0.,0.));
#4292=DIRECTION('',(1.,0.,0.));
#4293=DIRECTION('',(1.,0.,0.));
#4294=DIRECTION('center_axis',(1.,0.,0.));
#4295=DIRECTION('ref_axis',(0.,0.444750988585694,0.895654262621492));
#4296=DIRECTION('center_axis',(-1.,0.,0.));
#4297=DIRECTION('ref_axis',(0.,0.444750988585694,0.895654262621492));
#4298=DIRECTION('center_axis',(-1.,0.,0.));
#4299=DIRECTION('ref_axis',(0.,0.444750988585694,0.895654262621492));
#4300=DIRECTION('',(1.,0.,0.));
#4301=DIRECTION('',(1.,0.,0.));
#4302=DIRECTION('center_axis',(1.,0.,0.));
#4303=DIRECTION('ref_axis',(0.,-0.580623944517215,-0.814171870708679));
#4304=DIRECTION('center_axis',(-1.,0.,0.));
#4305=DIRECTION('ref_axis',(0.,-0.580623944517215,-0.814171870708679));
#4306=DIRECTION('center_axis',(-1.,0.,0.));
#4307=DIRECTION('ref_axis',(0.,-0.580623944517215,-0.814171870708679));
#4308=DIRECTION('center_axis',(0.,0.866025403784439,0.5));
#4309=DIRECTION('ref_axis',(0.,-0.5,0.866025403784439));
#4310=DIRECTION('',(0.,-0.5,0.866025403784439));
#4311=DIRECTION('',(1.,0.,0.));
#4312=DIRECTION('',(0.,-0.5,0.866025403784439));
#4313=DIRECTION('',(1.,0.,0.));
#4314=DIRECTION('center_axis',(0.,0.866025403784438,-0.5));
#4315=DIRECTION('ref_axis',(0.,0.5,0.866025403784438));
#4316=DIRECTION('',(0.,0.5,0.866025403784438));
#4317=DIRECTION('',(0.,0.5,0.866025403784438));
#4318=DIRECTION('',(1.,0.,0.));
#4319=DIRECTION('center_axis',(0.,-3.02823770847138E-16,-1.));
#4320=DIRECTION('ref_axis',(0.,1.,-3.02823770847138E-16));
#4321=DIRECTION('',(0.,1.,-3.02823770847138E-16));
#4322=DIRECTION('',(0.,1.,-3.02823770847138E-16));
#4323=DIRECTION('',(1.,0.,0.));
#4324=DIRECTION('center_axis',(0.,-0.866025403784439,-0.5));
#4325=DIRECTION('ref_axis',(0.,0.5,-0.866025403784439));
#4326=DIRECTION('',(0.,0.5,-0.866025403784439));
#4327=DIRECTION('',(0.,0.5,-0.866025403784439));
#4328=DIRECTION('',(1.,0.,0.));
#4329=DIRECTION('center_axis',(0.,-0.866025403784439,0.5));
#4330=DIRECTION('ref_axis',(0.,-0.5,-0.866025403784439));
#4331=DIRECTION('',(0.,-0.5,-0.866025403784439));
#4332=DIRECTION('',(0.,-0.5,-0.866025403784439));
#4333=DIRECTION('',(1.,0.,0.));
#4334=DIRECTION('center_axis',(0.,6.05647541694275E-16,1.));
#4335=DIRECTION('ref_axis',(0.,-1.,6.05647541694275E-16));
#4336=DIRECTION('',(0.,-1.,6.05647541694275E-16));
#4337=DIRECTION('',(0.,-1.,6.05647541694275E-16));
#4338=DIRECTION('center_axis',(1.,0.,0.));
#4339=DIRECTION('ref_axis',(0.,1.,0.));
#4340=DIRECTION('center_axis',(1.,0.,0.));
#4341=DIRECTION('ref_axis',(0.,1.,0.));
#5131=CARTESIAN_POINT('',(0.,0.,0.));
#5132=CARTESIAN_POINT('Ctrl Pts',(82.4430005297901,1.97158113240038,3.97043534620108));
#5133=CARTESIAN_POINT('Ctrl Pts',(88.2030005297901,1.97158113240038,3.97043534620108));
#5134=CARTESIAN_POINT('Ctrl Pts',(82.4430005297901,2.29671111436096,3.77621792657108));
#5135=CARTESIAN_POINT('Ctrl Pts',(88.2030005297901,2.29671111436096,3.77621792657108));
#5136=CARTESIAN_POINT('Ctrl Pts',(82.4430005297901,2.59552275281558,3.54102114079632));
#5137=CARTESIAN_POINT('Ctrl Pts',(88.2030005297901,2.59552275281558,3.54102114079632));
#5138=CARTESIAN_POINT('Ctrl Pts',(82.4430005297901,3.11908576775695,3.00435277140383));
#5139=CARTESIAN_POINT('Ctrl Pts',(88.2030005297901,3.11908576775695,3.00435277140383));
#5140=CARTESIAN_POINT('Ctrl Pts',(82.4430005297901,3.34301024132503,2.70651491388494));
#5141=CARTESIAN_POINT('Ctrl Pts',(88.2030005297901,3.34301024132503,2.70651491388494));
#5142=CARTESIAN_POINT('Ctrl Pts',(82.4430005297901,3.79251211736076,1.90981794028965));
#5143=CARTESIAN_POINT('Ctrl Pts',(88.2030005297901,3.79251211736076,1.90981794028965));
#5144=CARTESIAN_POINT('Ctrl Pts',(82.4430005297901,3.96610878107774,1.3893796287376));
#5145=CARTESIAN_POINT('Ctrl Pts',(88.2030005297901,3.96610878107774,1.3893796287376));
#5146=CARTESIAN_POINT('Ctrl Pts',(82.4430005297901,4.09877879619631,0.327978495265378));
#5147=CARTESIAN_POINT('Ctrl Pts',(88.2030005297901,4.09877879619631,0.327978495265378));
#5148=CARTESIAN_POINT('Ctrl Pts',(82.4430005297901,4.06307606785725,-0.201870082003989));
#5149=CARTESIAN_POINT('Ctrl Pts',(88.2030005297901,4.06307606785725,-0.201870082003989));
#5150=CARTESIAN_POINT('Ctrl Pts',(82.4430005297901,3.79206680758235,-1.20058842967181));
#5151=CARTESIAN_POINT('Ctrl Pts',(88.2030005297901,3.79206680758235,-1.20058842967181));
#5152=CARTESIAN_POINT('Ctrl Pts',(82.4430005297901,3.56572122172907,-1.66148594501202));
#5153=CARTESIAN_POINT('Ctrl Pts',(88.2030005297901,3.56572122172907,-1.66148594501202));
#5154=CARTESIAN_POINT('Ctrl Pts',(82.4430005297901,2.95711124459234,-2.45497912282895));
#5155=CARTESIAN_POINT('Ctrl Pts',(88.2030005297901,2.95711124459234,-2.45497912282895));
#5156=CARTESIAN_POINT('Ctrl Pts',(82.4430005297901,2.58595465431404,-2.78386901588456));
#5157=CARTESIAN_POINT('Ctrl Pts',(88.2030005297901,2.58595465431404,-2.78386901588456));
#5158=CARTESIAN_POINT('Ctrl Pts',(82.4430005297901,2.16151778945147,-3.03095833168073));
#5159=CARTESIAN_POINT('Ctrl Pts',(88.2030005297901,2.16151778945147,-3.03095833168073));
#5160=CARTESIAN_POINT('',(82.4430005297901,1.97158113240038,3.97043534620107));
#5161=CARTESIAN_POINT('',(82.4430005297901,2.16151778945147,-3.03095833168073));
#5162=CARTESIAN_POINT('Ctrl Pts',(82.4430005297901,1.97158113240038,3.97043534620108));
#5163=CARTESIAN_POINT('Ctrl Pts',(82.4430005297901,2.29671111436096,3.77621792657108));
#5164=CARTESIAN_POINT('Ctrl Pts',(82.4430005297901,2.59552275281558,3.54102114079632));
#5165=CARTESIAN_POINT('Ctrl Pts',(82.4430005297901,3.11908576775695,3.00435277140383));
#5166=CARTESIAN_POINT('Ctrl Pts',(82.4430005297901,3.34301024132503,2.70651491388494));
#5167=CARTESIAN_POINT('Ctrl Pts',(82.4430005297901,3.79251211736076,1.90981794028965));
#5168=CARTESIAN_POINT('Ctrl Pts',(82.4430005297901,3.96610878107774,1.3893796287376));
#5169=CARTESIAN_POINT('Ctrl Pts',(82.4430005297901,4.09877879619631,0.327978495265378));
#5170=CARTESIAN_POINT('Ctrl Pts',(82.4430005297901,4.06307606785725,-0.201870082003989));
#5171=CARTESIAN_POINT('Ctrl Pts',(82.4430005297901,3.79206680758235,-1.20058842967181));
#5172=CARTESIAN_POINT('Ctrl Pts',(82.4430005297901,3.56572122172907,-1.66148594501202));
#5173=CARTESIAN_POINT('Ctrl Pts',(82.4430005297901,2.95711124459234,-2.45497912282895));
#5174=CARTESIAN_POINT('Ctrl Pts',(82.4430005297901,2.58595465431404,-2.78386901588456));
#5175=CARTESIAN_POINT('Ctrl Pts',(82.4430005297901,2.16151778945147,-3.03095833168073));
#5176=CARTESIAN_POINT('',(86.4430005297901,2.16151778945147,-3.03095833168073));
#5177=CARTESIAN_POINT('',(82.4430005297901,2.16151778945147,-3.03095833168073));
#5178=CARTESIAN_POINT('',(86.4430005297901,1.97158113240038,3.97043534620107));
#5179=CARTESIAN_POINT('Ctrl Pts',(86.4430005297901,1.97158113240038,3.97043534620108));
#5180=CARTESIAN_POINT('Ctrl Pts',(86.4430005297901,2.29671111436096,3.77621792657108));
#5181=CARTESIAN_POINT('Ctrl Pts',(86.4430005297901,2.59552275281558,3.54102114079632));
#5182=CARTESIAN_POINT('Ctrl Pts',(86.4430005297901,3.11908576775695,3.00435277140383));
#5183=CARTESIAN_POINT('Ctrl Pts',(86.4430005297901,3.34301024132503,2.70651491388494));
#5184=CARTESIAN_POINT('Ctrl Pts',(86.4430005297901,3.79251211736076,1.90981794028965));
#5185=CARTESIAN_POINT('Ctrl Pts',(86.4430005297901,3.96610878107774,1.3893796287376));
#5186=CARTESIAN_POINT('Ctrl Pts',(86.4430005297901,4.09877879619631,0.327978495265378));
#5187=CARTESIAN_POINT('Ctrl Pts',(86.4430005297901,4.06307606785725,-0.201870082003989));
#5188=CARTESIAN_POINT('Ctrl Pts',(86.4430005297901,3.79206680758235,-1.20058842967181));
#5189=CARTESIAN_POINT('Ctrl Pts',(86.4430005297901,3.56572122172907,-1.66148594501202));
#5190=CARTESIAN_POINT('Ctrl Pts',(86.4430005297901,2.95711124459234,-2.45497912282895));
#5191=CARTESIAN_POINT('Ctrl Pts',(86.4430005297901,2.58595465431404,-2.78386901588456));
#5192=CARTESIAN_POINT('Ctrl Pts',(86.4430005297901,2.16151778945147,-3.03095833168073));
#5193=CARTESIAN_POINT('',(82.4430005297901,1.97158113240038,3.97043534620107));
#5194=CARTESIAN_POINT('Origin',(82.4430005297901,-2.77555756156289E-16,
5.55111512312578E-16));
#5195=CARTESIAN_POINT('',(82.4430005297901,-1.97158113240039,3.97043534620107));
#5196=CARTESIAN_POINT('Origin',(82.4430005297901,-2.77555756156289E-16,
5.55111512312578E-16));
#5197=CARTESIAN_POINT('',(86.4430005297901,-1.97158113240039,3.97043534620107));
#5198=CARTESIAN_POINT('Origin',(86.4430005297901,-2.77555756156289E-16,
5.55111512312578E-16));
#5199=CARTESIAN_POINT('',(82.4430005297901,-1.97158113240039,3.97043534620107));
#5200=CARTESIAN_POINT('Ctrl Pts',(82.4430005297901,-2.16151778945139,-3.03095833168078));
#5201=CARTESIAN_POINT('Ctrl Pts',(88.2030005297901,-2.16151778945139,-3.03095833168078));
#5202=CARTESIAN_POINT('Ctrl Pts',(82.4430005297901,-2.4417969811413,-2.86779155838698));
#5203=CARTESIAN_POINT('Ctrl Pts',(88.2030005297901,-2.4417969811413,-2.86779155838698));
#5204=CARTESIAN_POINT('Ctrl Pts',(82.4430005297901,-2.69946597133354,-2.66855779259647));
#5205=CARTESIAN_POINT('Ctrl Pts',(88.2030005297901,-2.69946597133354,-2.66855779259647));
#5206=CARTESIAN_POINT('Ctrl Pts',(82.4430005297901,-3.16313807023027,-2.20413689736136));
#5207=CARTESIAN_POINT('Ctrl Pts',(88.2030005297901,-3.16313807023027,-2.20413689736136));
#5208=CARTESIAN_POINT('Ctrl Pts',(82.4430005297901,-3.36582061002206,-1.93954623621156));
#5209=CARTESIAN_POINT('Ctrl Pts',(88.2030005297901,-3.36582061002206,-1.93954623621156));
#5210=CARTESIAN_POINT('Ctrl Pts',(82.4430005297901,-3.7905877946382,-1.20735040930033));
#5211=CARTESIAN_POINT('Ctrl Pts',(88.2030005297901,-3.7905877946382,-1.20735040930033));
#5212=CARTESIAN_POINT('Ctrl Pts',(82.4430005297901,-3.95787261855977,-0.715467908482556));
#5213=CARTESIAN_POINT('Ctrl Pts',(88.2030005297901,-3.95787261855977,-0.715467908482556));
#5214=CARTESIAN_POINT('Ctrl Pts',(82.4430005297901,-4.0999785741866,0.321696095215354));
#5215=CARTESIAN_POINT('Ctrl Pts',(88.2030005297901,-4.0999785741866,0.321696095215354));
#5216=CARTESIAN_POINT('Ctrl Pts',(82.4430005297901,-4.06691955087291,0.857794436836504));
#5217=CARTESIAN_POINT('Ctrl Pts',(88.2030005297901,-4.06691955087291,0.857794436836504));
#5218=CARTESIAN_POINT('Ctrl Pts',(82.4430005297901,-3.79581350913489,1.90493582172488));
#5219=CARTESIAN_POINT('Ctrl Pts',(88.2030005297901,-3.79581350913489,1.90493582172488));
#5220=CARTESIAN_POINT('Ctrl Pts',(82.4430005297901,-3.55404702294629,2.40416273654669));
#5221=CARTESIAN_POINT('Ctrl Pts',(88.2030005297901,-3.55404702294629,2.40416273654669));
#5222=CARTESIAN_POINT('Ctrl Pts',(82.4430005297901,-2.88474862400959,3.29779955123577));
#5223=CARTESIAN_POINT('Ctrl Pts',(88.2030005297901,-2.88474862400959,3.29779955123577));
#5224=CARTESIAN_POINT('Ctrl Pts',(82.4430005297901,-2.45846445810197,3.67959405679301));
#5225=CARTESIAN_POINT('Ctrl Pts',(88.2030005297901,-2.45846445810197,3.67959405679301));
#5226=CARTESIAN_POINT('Ctrl Pts',(82.4430005297901,-1.97158113240039,3.97043534620107));
#5227=CARTESIAN_POINT('Ctrl Pts',(88.2030005297901,-1.97158113240039,3.97043534620107));
#5228=CARTESIAN_POINT('',(82.4430005297901,-2.16151778945139,-3.03095833168078));
#5229=CARTESIAN_POINT('Ctrl Pts',(82.4430005297901,-2.16151778945139,-3.03095833168078));
#5230=CARTESIAN_POINT('Ctrl Pts',(82.4430005297901,-2.4417969811413,-2.86779155838698));
#5231=CARTESIAN_POINT('Ctrl Pts',(82.4430005297901,-2.69946597133354,-2.66855779259647));
#5232=CARTESIAN_POINT('Ctrl Pts',(82.4430005297901,-3.16313807023027,-2.20413689736136));
#5233=CARTESIAN_POINT('Ctrl Pts',(82.4430005297901,-3.36582061002206,-1.93954623621156));
#5234=CARTESIAN_POINT('Ctrl Pts',(82.4430005297901,-3.7905877946382,-1.20735040930033));
#5235=CARTESIAN_POINT('Ctrl Pts',(82.4430005297901,-3.95787261855977,-0.715467908482556));
#5236=CARTESIAN_POINT('Ctrl Pts',(82.4430005297901,-4.0999785741866,0.321696095215354));
#5237=CARTESIAN_POINT('Ctrl Pts',(82.4430005297901,-4.06691955087291,0.857794436836504));
#5238=CARTESIAN_POINT('Ctrl Pts',(82.4430005297901,-3.79581350913489,1.90493582172488));
#5239=CARTESIAN_POINT('Ctrl Pts',(82.4430005297901,-3.55404702294629,2.40416273654669));
#5240=CARTESIAN_POINT('Ctrl Pts',(82.4430005297901,-2.88474862400959,3.29779955123577));
#5241=CARTESIAN_POINT('Ctrl Pts',(82.4430005297901,-2.45846445810197,3.67959405679301));
#5242=CARTESIAN_POINT('Ctrl Pts',(82.4430005297901,-1.97158113240039,3.97043534620107));
#5243=CARTESIAN_POINT('',(86.4430005297901,-2.16151778945139,-3.03095833168078));
#5244=CARTESIAN_POINT('Ctrl Pts',(86.4430005297901,-2.16151778945139,-3.03095833168078));
#5245=CARTESIAN_POINT('Ctrl Pts',(86.4430005297901,-2.4417969811413,-2.86779155838698));
#5246=CARTESIAN_POINT('Ctrl Pts',(86.4430005297901,-2.69946597133354,-2.66855779259647));
#5247=CARTESIAN_POINT('Ctrl Pts',(86.4430005297901,-3.16313807023027,-2.20413689736136));
#5248=CARTESIAN_POINT('Ctrl Pts',(86.4430005297901,-3.36582061002206,-1.93954623621156));
#5249=CARTESIAN_POINT('Ctrl Pts',(86.4430005297901,-3.7905877946382,-1.20735040930033));
#5250=CARTESIAN_POINT('Ctrl Pts',(86.4430005297901,-3.95787261855977,-0.715467908482556));
#5251=CARTESIAN_POINT('Ctrl Pts',(86.4430005297901,-4.0999785741866,0.321696095215354));
#5252=CARTESIAN_POINT('Ctrl Pts',(86.4430005297901,-4.06691955087291,0.857794436836504));
#5253=CARTESIAN_POINT('Ctrl Pts',(86.4430005297901,-3.79581350913489,1.90493582172488));
#5254=CARTESIAN_POINT('Ctrl Pts',(86.4430005297901,-3.55404702294629,2.40416273654669));
#5255=CARTESIAN_POINT('Ctrl Pts',(86.4430005297901,-2.88474862400959,3.29779955123577));
#5256=CARTESIAN_POINT('Ctrl Pts',(86.4430005297901,-2.45846445810197,3.67959405679301));
#5257=CARTESIAN_POINT('Ctrl Pts',(86.4430005297901,-1.97158113240039,3.97043534620107));
#5258=CARTESIAN_POINT('',(82.4430005297901,-2.16151778945139,-3.03095833168078));
#5259=CARTESIAN_POINT('Origin',(82.4430005297901,-2.77555756156289E-16,
5.55111512312578E-16));
#5260=CARTESIAN_POINT('Origin',(82.4430005297901,-2.77555756156289E-16,
5.55111512312578E-16));
#5261=CARTESIAN_POINT('Origin',(86.4430005297901,-2.77555756156289E-16,
5.55111512312578E-16));
#5262=CARTESIAN_POINT('Origin',(82.4430005297901,7.33246945257534,-3.33066907387547E-15));
#5263=CARTESIAN_POINT('',(82.4430005297901,7.33246945257534,-3.33066907387547E-15));
#5264=CARTESIAN_POINT('',(82.4430005297901,3.66623472628768,6.35010481840362));
#5265=CARTESIAN_POINT('',(82.4430005297901,7.33246945257534,-3.33066907387547E-15));
#5266=CARTESIAN_POINT('',(86.4430005297901,3.66623472628768,6.35010481840362));
#5267=CARTESIAN_POINT('',(82.4430005297901,3.66623472628768,6.35010481840362));
#5268=CARTESIAN_POINT('',(86.4430005297901,7.33246945257534,-3.33066907387547E-15));
#5269=CARTESIAN_POINT('',(86.4430005297901,7.33246945257534,-3.33066907387547E-15));
#5270=CARTESIAN_POINT('',(82.4430005297901,7.33246945257534,-3.33066907387547E-15));
#5271=CARTESIAN_POINT('Origin',(82.4430005297901,3.66623472628767,-6.35010481840363));
#5272=CARTESIAN_POINT('',(82.4430005297901,3.66623472628767,-6.35010481840363));
#5273=CARTESIAN_POINT('',(82.4430005297901,3.66623472628767,-6.35010481840363));
#5274=CARTESIAN_POINT('',(86.4430005297901,3.66623472628767,-6.35010481840363));
#5275=CARTESIAN_POINT('',(86.4430005297901,3.66623472628767,-6.35010481840363));
#5276=CARTESIAN_POINT('',(82.4430005297901,3.66623472628767,-6.35010481840363));
#5277=CARTESIAN_POINT('Origin',(82.4430005297901,-3.66623472628767,-6.35010481840362));
#5278=CARTESIAN_POINT('',(82.4430005297901,-3.66623472628767,-6.35010481840362));
#5279=CARTESIAN_POINT('',(82.4430005297901,-3.66623472628767,-6.35010481840362));
#5280=CARTESIAN_POINT('',(86.4430005297901,-3.66623472628767,-6.35010481840362));
#5281=CARTESIAN_POINT('',(86.4430005297901,-3.66623472628767,-6.35010481840362));
#5282=CARTESIAN_POINT('',(82.4430005297901,-3.66623472628767,-6.35010481840362));
#5283=CARTESIAN_POINT('Origin',(82.4430005297901,-7.33246945257535,2.77555756156289E-15));
#5284=CARTESIAN_POINT('',(82.4430005297901,-7.33246945257535,2.77555756156289E-15));
#5285=CARTESIAN_POINT('',(82.4430005297901,-7.33246945257535,2.77555756156289E-15));
#5286=CARTESIAN_POINT('',(86.4430005297901,-7.33246945257535,2.77555756156289E-15));
#5287=CARTESIAN_POINT('',(86.4430005297901,-7.33246945257535,2.77555756156289E-15));
#5288=CARTESIAN_POINT('',(82.4430005297901,-7.33246945257535,2.77555756156289E-15));
#5289=CARTESIAN_POINT('Origin',(82.4430005297901,-3.66623472628767,6.35010481840363));
#5290=CARTESIAN_POINT('',(82.4430005297901,-3.66623472628767,6.35010481840363));
#5291=CARTESIAN_POINT('',(82.4430005297901,-3.66623472628767,6.35010481840363));
#5292=CARTESIAN_POINT('',(86.4430005297901,-3.66623472628767,6.35010481840363));
#5293=CARTESIAN_POINT('',(86.4430005297901,-3.66623472628767,6.35010481840363));
#5294=CARTESIAN_POINT('',(82.4430005297901,-3.66623472628767,6.35010481840363));
#5295=CARTESIAN_POINT('Origin',(82.4430005297901,3.66623472628768,6.35010481840362));
#5296=CARTESIAN_POINT('',(82.4430005297901,3.66623472628768,6.35010481840362));
#5297=CARTESIAN_POINT('',(86.4430005297901,3.66623472628768,6.35010481840362));
#5298=CARTESIAN_POINT('Origin',(86.4430005297901,0.,0.));
#5299=CARTESIAN_POINT('Origin',(82.4430005297901,0.,0.));
#27685=UNCERTAINTY_MEASURE_WITH_UNIT(LENGTH_MEASURE(0.01),#27708,
'DISTANCE_ACCURACY_VALUE',
'Maximum model space distance between geometric entities at asserted c
onnectivities');
#27695=UNCERTAINTY_MEASURE_WITH_UNIT(LENGTH_MEASURE(0.01),#27708,
'DISTANCE_ACCURACY_VALUE',
'Maximum model space distance between geometric entities at asserted c
onnectivities');
#27697=(
GEOMETRIC_REPRESENTATION_CONTEXT(3)
GLOBAL_UNCERTAINTY_ASSIGNED_CONTEXT((#27685))
GLOBAL_UNIT_ASSIGNED_CONTEXT((#27708,#27710,#27711))
REPRESENTATION_CONTEXT('','3D')
);
#27707=(
GEOMETRIC_REPRESENTATION_CONTEXT(3)
GLOBAL_UNCERTAINTY_ASSIGNED_CONTEXT((#27695))
GLOBAL_UNIT_ASSIGNED_CONTEXT((#27708,#27710,#27711))
REPRESENTATION_CONTEXT('','3D')
);
#27708=(
LENGTH_UNIT()
NAMED_UNIT(*)
SI_UNIT(.MILLI.,.METRE.)
);
#27710=(
NAMED_UNIT(*)
PLANE_ANGLE_UNIT()
SI_UNIT($,.RADIAN.)
);
#27711=(
NAMED_UNIT(*)
SI_UNIT($,.STERADIAN.)
SOLID_ANGLE_UNIT()
);
#27713=SHAPE_DEFINITION_REPRESENTATION(#27724,#27745);
#27724=PRODUCT_DEFINITION_SHAPE('',$,#27757);
#27745=SHAPE_REPRESENTATION('',(#3956),#27697);
#27755=PRODUCT_DEFINITION_CONTEXT('part definition',#27790,'design');
#27757=PRODUCT_DEFINITION('Nut_01','Nut_01',#27768,#27755);
#27768=PRODUCT_DEFINITION_FORMATION('',$,#27793);
#27790=APPLICATION_CONTEXT(
'Core Data for Automotive Mechanical Design Process');
#27791=PRODUCT_CONTEXT('part definition',#27790,'mechanical');
#27793=PRODUCT('Nut_01','Nut_01',$,(#27791));
#27804=PRESENTATION_STYLE_ASSIGNMENT((#27806));
#27806=SURFACE_STYLE_USAGE(.BOTH.,#27808);
#27808=SURFACE_SIDE_STYLE('',(#27810));
#27810=SURFACE_STYLE_FILL_AREA(#27812);
#27812=FILL_AREA_STYLE('Opaque(160,160,160)',(#27814));
#27814=FILL_AREA_STYLE_COLOUR('Opaque(160,160,160)',#27816);
#27816=COLOUR_RGB('Opaque(160,160,160)', 0.09019608, 0.27058824, 0.51372549);
ENDSEC;
END-ISO-10303-21;
